ISO-10303-21;
HEADER;
FILE_DESCRIPTION (('STEP AP214'),
    '1' );
FILE_NAME ('socket head cap screw_iso_ISO 4762 M5 x 16 - 16N.step',
    '2026-10-08T11:45:07',
    ( '' ),
    ( '' ),
    'SwSTEP 2.0',
    'SolidWorks 2026',
    '' );
FILE_SCHEMA (( 'AUTOMOTIVE_DESIGN' ));
ENDSEC;

DATA;
#21=CARTESIAN_POINT ( 'NONE',  ( 0.000000000000000000, -2.357898499370432166, 3.035766082959412415E-15 ) ) ;
#49=EDGE_LOOP ( 'NONE', ( #22549, #9625, #3734, #25351, #25610, #29887 ) ) ;
#82=DIRECTION ( 'NONE',  ( 0.000000000000000000, -1.000000000000000000, 1.287488025362403787E-15 ) ) ;
#97=AXIS2_PLACEMENT_3D ( 'NONE', #25295, #22018, #38332 ) ;
#112=MANIFOLD_SOLID_BREP ( 'Hex', #10772 ) ;
#220=STYLED_ITEM ( 'NONE', ( #39718 ), #29693 ) ;
#226=EDGE_CURVE ( 'NONE', #9576, #14223, #10277, .T. ) ;
#268=VECTOR ( 'NONE', #36102, 1000.000000000000000 ) ;
#323=LINE ( 'NONE', #26764, #22557 ) ;
#398=AXIS2_PLACEMENT_3D ( 'NONE', #38815, #39023, #34911 ) ;
#495=ADVANCED_FACE ( 'NONE', ( #34696 ), #4808, .T. ) ;
#831=ORIENTED_EDGE ( 'NONE', *, *, #7767, .F. ) ;
#931=EDGE_CURVE ( 'NONE', #37795, #12884, #15890, .T. ) ;
#967=VERTEX_POINT ( 'NONE', #5404 ) ;
#1142=ORIENTED_EDGE ( 'NONE', *, *, #23345, .T. ) ;
#1203=PRODUCT_DEFINITION_CONTEXT ( 'detailed design', #5815, 'design' ) ;
#1494=CARTESIAN_POINT ( 'NONE',  ( 2.500000000000000000, -1.178949249685218748, -2.041999999999998039 ) ) ;
#1497=CARTESIAN_POINT ( 'NONE',  ( 2.500000000000000000, 1.768423874527822459, -1.021000000000002794 ) ) ;
#1625=( LENGTH_UNIT ( ) NAMED_UNIT ( * ) SI_UNIT ( .MILLI., .METRE. ) );
#1696=DIRECTION ( 'NONE',  ( 0.000000000000000000, 0.000000000000000000, 1.000000000000000000 ) ) ;
#1766=EDGE_CURVE ( 'NONE', #20507, #33396, #18698, .T. ) ;
#1780=DIRECTION ( 'NONE',  ( -1.000000000000000000, -0.000000000000000000, -0.000000000000000000 ) ) ;
#1827=CARTESIAN_POINT ( 'NONE',  ( 21.00000000000000355, 0.000000000000000000, 0.000000000000000000 ) ) ;
#1843=ORIENTED_EDGE ( 'NONE', *, *, #23082, .T. ) ;
#1869=ORIENTED_EDGE ( 'NONE', *, *, #10489, .T. ) ;
#1871=CARTESIAN_POINT ( 'NONE',  ( -31.74999999999995737, 5.204748896376250699E-16, -4.250000000000000000 ) ) ;
#1952=CARTESIAN_POINT ( 'NONE',  ( 2.500000000000000000, 1.768423874527823791, 1.020999999999998353 ) ) ;
#2092=DIRECTION ( 'NONE',  ( -1.000000000000000000, -0.000000000000000000, -0.000000000000000000 ) ) ;
#2127=ADVANCED_FACE ( 'NONE', ( #32128 ), #39080, .F. ) ;
#2140=ORIENTED_EDGE ( 'NONE', *, *, #4828, .T. ) ;
#2321=( GEOMETRIC_REPRESENTATION_CONTEXT ( 3 ) GLOBAL_UNCERTAINTY_ASSIGNED_CONTEXT ( ( #2360 ) ) GLOBAL_UNIT_ASSIGNED_CONTEXT ( ( #25403, #39085, #28871 ) ) REPRESENTATION_CONTEXT ( 'NONE', 'WORKASPACE' ) );
#2346=( NAMED_UNIT ( * ) PLANE_ANGLE_UNIT ( ) SI_UNIT ( $, .RADIAN. ) );
#2357=VECTOR ( 'NONE', #29659, 1000.000000000000000 ) ;
#2360=UNCERTAINTY_MEASURE_WITH_UNIT (LENGTH_MEASURE( 1.000000000000000082E-05 ), #25403, 'distance_accuracy_value', 'NONE');
#2387=ORIENTED_EDGE ( 'NONE', *, *, #25882, .T. ) ;
#2520=ORIENTED_EDGE ( 'NONE', *, *, #10182, .F. ) ;
#2531=CARTESIAN_POINT ( 'NONE',  ( 2.500000000000000000, 2.357898499370431722, -2.818925648462311528E-15 ) ) ;
#2555=ADVANCED_FACE ( 'NONE', ( #2743 ), #9953, .F. ) ;
#2629=( NAMED_UNIT ( * ) PLANE_ANGLE_UNIT ( ) SI_UNIT ( $, .RADIAN. ) );
#2716=DIRECTION ( 'NONE',  ( 0.000000000000000000, -1.000000000000000000, 1.287488025362403787E-15 ) ) ;
#2743=FACE_OUTER_BOUND ( 'NONE', #9885, .T. ) ;
#2770=ORIENTED_EDGE ( 'NONE', *, *, #42290, .F. ) ;
#2776=EDGE_LOOP ( 'NONE', ( #27954, #37139, #41972, #27995 ) ) ;
#2816=DIRECTION ( 'NONE',  ( 1.000000000000000000, 0.000000000000000000, 0.000000000000000000 ) ) ;
#2823=EDGE_LOOP ( 'NONE', ( #25792, #29092 ) ) ;
#2968=DIRECTION ( 'NONE',  ( 0.000000000000000000, -1.000000000000000000, 0.000000000000000000 ) ) ;
#2995=( GEOMETRIC_REPRESENTATION_CONTEXT ( 3 ) GLOBAL_UNCERTAINTY_ASSIGNED_CONTEXT ( ( #35544 ) ) GLOBAL_UNIT_ASSIGNED_CONTEXT ( ( #36447, #2346, #42771 ) ) REPRESENTATION_CONTEXT ( 'NONE', 'WORKASPACE' ) );
#3037=CARTESIAN_POINT ( 'NONE',  ( 5.200000000000002842, 3.061616997868383634E-16, -2.500000000000000444 ) ) ;
#3050=SHAPE_REPRESENTATION_RELATIONSHIP ( 'NONE' , 'NONE' ,  #18009, #29693 ) ;
#3127=LINE ( 'NONE', #29163, #268 ) ;
#3202=ORIENTED_EDGE ( 'NONE', *, *, #24497, .F. ) ;
#3241=DIRECTION ( 'NONE',  ( 0.000000000000000000, 0.000000000000000000, 1.000000000000000000 ) ) ;
#3337=CARTESIAN_POINT ( 'NONE',  ( 4.999999999999997335, 0.000000000000000000, 0.000000000000000000 ) ) ;
#3346=EDGE_CURVE ( 'NONE', #24569, #21049, #5887, .T. ) ;
#3450=DIRECTION ( 'NONE',  ( 0.000000000000000000, 0.000000000000000000, -1.000000000000000000 ) ) ;
#3530=LINE ( 'NONE', #23669, #14622 ) ;
#3607=PRODUCT ( 'socket head cap screw_iso_ISO 4762 M5 x 16 - 16N', 'socket head cap screw_iso_ISO 4762 M5 x 16 - 16N', '', ( #18613 ) ) ;
#3642=ORIENTED_EDGE ( 'NONE', *, *, #35108, .T. ) ;
#3647=DIRECTION ( 'NONE',  ( 0.000000000000000000, 0.000000000000000000, 1.000000000000000000 ) ) ;
#3648=DIRECTION ( 'NONE',  ( 0.000000000000000000, 0.000000000000000000, 1.000000000000000000 ) ) ;
#3686=DIRECTION ( 'NONE',  ( 0.000000000000000000, -0.4999999999999989453, 0.8660254037844391517 ) ) ;
#3734=ORIENTED_EDGE ( 'NONE', *, *, #34726, .T. ) ;
#3780=ORIENTED_EDGE ( 'NONE', *, *, #931, .F. ) ;
#3805=DIRECTION ( 'NONE',  ( -1.000000000000000000, -0.000000000000000000, -0.000000000000000000 ) ) ;
#3852=CARTESIAN_POINT ( 'NONE',  ( 0.000000000000000000, 0.000000000000000000, 0.000000000000000000 ) ) ;
#3961=DIRECTION ( 'NONE',  ( 0.000000000000000000, 0.5000000000000011102, 0.8660254037844379305 ) ) ;
#4090=CARTESIAN_POINT ( 'NONE',  ( 2.500000000000000000, -1.178949249685214307, 2.042000000000001592 ) ) ;
#4132=ORIENTED_EDGE ( 'NONE', *, *, #931, .T. ) ;
#4204=EDGE_CURVE ( 'NONE', #34610, #24569, #5993, .T. ) ;
#4220=LINE ( 'NONE', #30863, #26175 ) ;
#4308=VERTEX_POINT ( 'NONE', #11864 ) ;
#4377=FACE_OUTER_BOUND ( 'NONE', #2776, .T. ) ;
#4380=PRODUCT_DEFINITION ( 'UNKNOWN', '', #37904, #1203 ) ;
#4390=ORIENTED_EDGE ( 'NONE', *, *, #10873, .T. ) ;
#4475=CARTESIAN_POINT ( 'NONE',  ( 0.000000000000000000, 0.000000000000000000, 4.000000000000000000 ) ) ;
#4493=FACE_OUTER_BOUND ( 'NONE', #30512, .T. ) ;
#4533=ORIENTED_EDGE ( 'NONE', *, *, #36202, .T. ) ;
#4553=DIRECTION ( 'NONE',  ( 0.000000000000000000, 0.000000000000000000, 1.000000000000000000 ) ) ;
#4562=AXIS2_PLACEMENT_3D ( 'NONE', #5825, #29200, #32666 ) ;
#4670=EDGE_CURVE ( 'NONE', #37795, #12005, #36342, .T. ) ;
#4677=DIRECTION ( 'NONE',  ( 0.000000000000000000, -0.8660254037844390407, -0.4999999999999993339 ) ) ;
#4678=CARTESIAN_POINT ( 'NONE',  ( -31.74999999999995737, 3.061616997868383634E-16, -2.500000000000000444 ) ) ;
#4691=SURFACE_STYLE_FILL_AREA ( #14548 ) ;
#4808=PLANE ( 'NONE',  #31670 ) ;
#4828=EDGE_CURVE ( 'NONE', #32170, #30953, #20041, .T. ) ;
#4851=CIRCLE ( 'NONE', #38198, 4.000000000000000000 ) ;
#4913=SURFACE_SIDE_STYLE ('',( #4691 ) ) ;
#4958=FACE_OUTER_BOUND ( 'NONE', #37130, .T. ) ;
#4977=EDGE_LOOP ( 'NONE', ( #24117, #35600, #37362, #16666, #4390 ) ) ;
#4985=CARTESIAN_POINT ( 'NONE',  ( 0.2500000000000002220, 0.000000000000000000, 0.000000000000000000 ) ) ;
#5064=EDGE_CURVE ( 'NONE', #12884, #10324, #15433, .T. ) ;
#5404=CARTESIAN_POINT ( 'NONE',  ( 20.55500000000001748, 0.000000000000000000, 2.500000000000000888 ) ) ;
#5458=CARTESIAN_POINT ( 'NONE',  ( 2.500000000000000000, -2.357898499370432166, 3.035766082959412415E-15 ) ) ;
#5474=AXIS2_PLACEMENT_3D ( 'NONE', #39378, #19792, #33058 ) ;
#5495=EDGE_LOOP ( 'NONE', ( #13359, #6931, #18177, #33037 ) ) ;
#5541=LINE ( 'NONE', #29117, #9597 ) ;
#5611=VECTOR ( 'NONE', #12186, 1000.000000000000000 ) ;
#5815=APPLICATION_CONTEXT ( 'automotive_design' ) ;
#5825=CARTESIAN_POINT ( 'NONE',  ( 2.500000000000000000, 2.357898499370431722, -2.818925648462311528E-15 ) ) ;
#5887=CIRCLE ( 'NONE', #30294, 2.700000000000000622 ) ;
#5993=CIRCLE ( 'NONE', #36656, 0.2000000000000000944 ) ;
#6036=TOROIDAL_SURFACE ( 'NONE', #30435, 2.700000000000000622, 0.2000000000000000111 ) ;
#6229=FACE_BOUND ( 'NONE', #2823, .T. ) ;
#6608=MECHANICAL_DESIGN_GEOMETRIC_PRESENTATION_REPRESENTATION('',(#28942),#28266);
#6703=DIRECTION ( 'NONE',  ( 0.000000000000000000, 0.000000000000000000, -1.000000000000000000 ) ) ;
#6718=EDGE_CURVE ( 'NONE', #29708, #26637, #20634, .T. ) ;
#6741=DIRECTION ( 'NONE',  ( 1.000000000000000000, 0.000000000000000000, 0.000000000000000000 ) ) ;
#6765=ORIENTED_EDGE ( 'NONE', *, *, #4670, .T. ) ;
#6766=AXIS2_PLACEMENT_3D ( 'NONE', #21096, #4677, #24362 ) ;
#6799=DIRECTION ( 'NONE',  ( 0.000000000000000000, 0.000000000000000000, -1.000000000000000000 ) ) ;
#6801=CIRCLE ( 'NONE', #31216, 4.250000000000000000 ) ;
#6931=ORIENTED_EDGE ( 'NONE', *, *, #22927, .T. ) ;
#6958=ORIENTED_EDGE ( 'NONE', *, *, #19279, .T. ) ;
#7071=DIRECTION ( 'NONE',  ( -0.5000000000000051070, 1.060575238724903217E-16, -0.8660254037844355990 ) ) ;
#7489=DIRECTION ( 'NONE',  ( 0.000000000000000000, 0.000000000000000000, 1.000000000000000000 ) ) ;
#7611=VECTOR ( 'NONE', #30163, 1000.000000000000000 ) ;
#7767=EDGE_CURVE ( 'NONE', #41990, #11322, #34871, .T. ) ;
#7926=DIRECTION ( 'NONE',  ( 0.000000000000000000, 0.000000000000000000, -1.000000000000000000 ) ) ;
#8047=DIRECTION ( 'NONE',  ( 0.000000000000000000, 0.000000000000000000, 1.000000000000000000 ) ) ;
#8139=VERTEX_POINT ( 'NONE', #30925 ) ;
#8205=ORIENTED_EDGE ( 'NONE', *, *, #20565, .T. ) ;
#8256=AXIS2_PLACEMENT_3D ( 'NONE', #32891, #2968, #6703 ) ;
#8383=DIRECTION ( 'NONE',  ( -1.000000000000000000, -0.000000000000000000, -0.000000000000000000 ) ) ;
#8396=ORIENTED_EDGE ( 'NONE', *, *, #29483, .T. ) ;
#8537=CARTESIAN_POINT ( 'NONE',  ( 2.500000000000000000, 2.357898499370431722, -2.818925648462311528E-15 ) ) ;
#8563=DIRECTION ( 'NONE',  ( 0.000000000000000000, 0.000000000000000000, -1.000000000000000000 ) ) ;
#8730=DIRECTION ( 'NONE',  ( 0.000000000000000000, 0.000000000000000000, -1.000000000000000000 ) ) ;
#8748=AXIS2_PLACEMENT_3D ( 'NONE', #23366, #20114, #28682 ) ;
#8801=CARTESIAN_POINT ( 'NONE',  ( 0.2500000000000002220, 0.000000000000000000, 0.000000000000000000 ) ) ;
#8895=CARTESIAN_POINT ( 'NONE',  ( 2.500000000000000000, 0.000000000000000000, 0.000000000000000000 ) ) ;
#9067=ORIENTED_EDGE ( 'NONE', *, *, #40856, .T. ) ;
#9138=EDGE_LOOP ( 'NONE', ( #26067, #2140, #9267, #4132, #36040 ) ) ;
#9267=ORIENTED_EDGE ( 'NONE', *, *, #41442, .T. ) ;
#9285=EDGE_CURVE ( 'NONE', #967, #21211, #41262, .T. ) ;
#9298=ORIENTED_EDGE ( 'NONE', *, *, #20565, .F. ) ;
#9363=CARTESIAN_POINT ( 'NONE',  ( 2.500000000000000000, -1.768423874527825568, -1.020999999999998575 ) ) ;
#9537=CARTESIAN_POINT ( 'NONE',  ( 4.999999999999997335, 0.000000000000000000, 4.250000000000000000 ) ) ;
#9576=VERTEX_POINT ( 'NONE', #27900 ) ;
#9578=LINE ( 'NONE', #13514, #2357 ) ;
#9597=VECTOR ( 'NONE', #32156, 1000.000000000000114 ) ;
#9618=DIRECTION ( 'NONE',  ( 0.000000000000000000, 0.000000000000000000, -1.000000000000000000 ) ) ;
#9625=ORIENTED_EDGE ( 'NONE', *, *, #11978, .F. ) ;
#9642=CARTESIAN_POINT ( 'NONE',  ( 2.500000000000000000, 1.178949249685212974, -2.042000000000001148 ) ) ;
#9716=CARTESIAN_POINT ( 'NONE',  ( 5.000000000000002665, 3.306546357697854226E-16, 2.700000000000000622 ) ) ;
#9885=EDGE_LOOP ( 'NONE', ( #19166, #9067, #37262 ) ) ;
#9939=EDGE_LOOP ( 'NONE', ( #38032, #32165, #3780 ) ) ;
#9953=PLANE ( 'NONE',  #4562 ) ;
#10036=DIRECTION ( 'NONE',  ( -1.000000000000000000, -0.000000000000000000, -0.000000000000000000 ) ) ;
#10076=DIRECTION ( 'NONE',  ( 0.000000000000000000, 0.000000000000000000, -1.000000000000000000 ) ) ;
#10146=LINE ( 'NONE', #36531, #29173 ) ;
#10182=EDGE_CURVE ( 'NONE', #42638, #8139, #14713, .T. ) ;
#10213=DIRECTION ( 'NONE',  ( 1.000000000000000000, 0.000000000000000000, 0.000000000000000000 ) ) ;
#10277=LINE ( 'NONE', #39919, #36560 ) ;
#10324=VERTEX_POINT ( 'NONE', #26702 ) ;
#10489=EDGE_CURVE ( 'NONE', #32708, #41990, #27568, .T. ) ;
#10753=ADVANCED_FACE ( 'NONE', ( #23187 ), #21745, .F. ) ;
#10772=CLOSED_SHELL ( 'NONE', ( #16756, #37070, #10753, #19122, #13608, #14632, #42849, #23887, #22527, #36414, #28197, #32775, #14167, #15893, #35306, #37849, #495, #37388, #2127, #23340, #29798, #19848, #2555, #21060, #42130, #16147, #24486 ) ) ;
#10833=VERTEX_POINT ( 'NONE', #3037 ) ;
#10873=EDGE_CURVE ( 'NONE', #11322, #30953, #14777, .T. ) ;
#10893=CIRCLE ( 'NONE', #12982, 0.2500000000000002220 ) ;
#10932=CARTESIAN_POINT ( 'NONE',  ( 2.500000000000000000, 2.357898499370431722, -2.818925648462311528E-15 ) ) ;
#10942=VECTOR ( 'NONE', #3805, 1000.000000000000000 ) ;
#10968=DIRECTION ( 'NONE',  ( 0.000000000000000000, -0.5000000000000013323, -0.8660254037844380415 ) ) ;
#10975=ORIENTED_EDGE ( 'NONE', *, *, #9285, .F. ) ;
#10977=FACE_OUTER_BOUND ( 'NONE', #28803, .T. ) ;
#11082=DIRECTION ( 'NONE',  ( -1.000000000000000000, -0.000000000000000000, -0.000000000000000000 ) ) ;
#11089=ORIENTED_EDGE ( 'NONE', *, *, #42290, .T. ) ;
#11099=VECTOR ( 'NONE', #14690, 1000.000000000000000 ) ;
#11180=VECTOR ( 'NONE', #42796, 1000.000000000000000 ) ;
#11322=VERTEX_POINT ( 'NONE', #36047 ) ;
#11340=DIRECTION ( 'NONE',  ( 0.000000000000000000, -0.5000000000000013323, -0.8660254037844380415 ) ) ;
#11422=EDGE_LOOP ( 'NONE', ( #18439, #19575, #1869, #6958, #4533 ) ) ;
#11567=DIRECTION ( 'NONE',  ( -1.000000000000000000, -0.000000000000000000, -0.000000000000000000 ) ) ;
#11633=AXIS2_PLACEMENT_3D ( 'NONE', #8895, #15273, #28349 ) ;
#11653=DIRECTION ( 'NONE',  ( 1.000000000000000000, 0.000000000000000000, 0.000000000000000000 ) ) ;
#11812=PLANE ( 'NONE',  #13273 ) ;
#11864=CARTESIAN_POINT ( 'NONE',  ( 0.000000000000000000, -1.178949249685214307, 2.042000000000001592 ) ) ;
#11959=CARTESIAN_POINT ( 'NONE',  ( 21.00000000000000355, 0.000000000000000000, 0.000000000000000000 ) ) ;
#11978=EDGE_CURVE ( 'NONE', #4308, #14223, #28316, .T. ) ;
#12005=VERTEX_POINT ( 'NONE', #38097 ) ;
#12108=EDGE_CURVE ( 'NONE', #28770, #22696, #3127, .T. ) ;
#12121=DIRECTION ( 'NONE',  ( 0.000000000000000000, 0.000000000000000000, 1.000000000000000000 ) ) ;
#12186=DIRECTION ( 'NONE',  ( 0.000000000000000000, -0.4999999999999993339, 0.8660254037844390407 ) ) ;
#12286=DIRECTION ( 'NONE',  ( 0.000000000000000000, 1.224646799147353207E-16, 1.000000000000000000 ) ) ;
#12379=CARTESIAN_POINT ( 'NONE',  ( 5.000000000000000888, 4.250000000000000000, 0.000000000000000000 ) ) ;
#12441=CARTESIAN_POINT ( 'NONE',  ( 20.55500000000001748, 0.000000000000000000, 0.000000000000000000 ) ) ;
#12633=ORIENTED_EDGE ( 'NONE', *, *, #5064, .F. ) ;
#12757=DIRECTION ( 'NONE',  ( -1.000000000000000000, -0.000000000000000000, -0.000000000000000000 ) ) ;
#12776=DIRECTION ( 'NONE',  ( -0.000000000000000000, 0.000000000000000000, 1.000000000000000000 ) ) ;
#12827=COLOUR_RGB ( '', 0.09019608, 0.27058824, 0.51372549) ;
#12875=AXIS2_PLACEMENT_3D ( 'NONE', #9642, #39505, #22343 ) ;
#12884=VERTEX_POINT ( 'NONE', #1497 ) ;
#12899=PLANE ( 'NONE',  #40362 ) ;
#12905=CARTESIAN_POINT ( 'NONE',  ( 2.500000000000000000, -1.178949249685218748, -2.041999999999998039 ) ) ;
#12958=CIRCLE ( 'NONE', #18571, 2.500000000000000444 ) ;
#12982=AXIS2_PLACEMENT_3D ( 'NONE', #40828, #14252, #34508 ) ;
#13154=VECTOR ( 'NONE', #32786, 1000.000000000000114 ) ;
#13163=CARTESIAN_POINT ( 'NONE',  ( 2.500000000000000000, 2.357898499370431722, -2.818925648462311528E-15 ) ) ;
#13260=DIRECTION ( 'NONE',  ( -1.000000000000000000, -0.000000000000000000, -0.000000000000000000 ) ) ;
#13273=AXIS2_PLACEMENT_3D ( 'NONE', #25137, #35113, #15313 ) ;
#13314=ORIENTED_EDGE ( 'NONE', *, *, #31463, .T. ) ;
#13359=ORIENTED_EDGE ( 'NONE', *, *, #9285, .T. ) ;
#13466=AXIS2_PLACEMENT_3D ( 'NONE', #26824, #6741, #3450 ) ;
#13514=CARTESIAN_POINT ( 'NONE',  ( 0.000000000000000000, 1.178949249685212974, -2.042000000000001148 ) ) ;
#13549=ORIENTED_EDGE ( 'NONE', *, *, #24497, .T. ) ;
#13552=AXIS2_PLACEMENT_3D ( 'NONE', #3852, #14597, #10213 ) ;
#13565=PLANE ( 'NONE',  #29964 ) ;
#13582=FILL_AREA_STYLE ('',( #32760 ) ) ;
#13608=ADVANCED_FACE ( 'NONE', ( #31708 ), #28667, .T. ) ;
#13744=ORIENTED_EDGE ( 'NONE', *, *, #18614, .F. ) ;
#13789=DIRECTION ( 'NONE',  ( 0.000000000000000000, -0.5000000000000009992, -0.8660254037844380415 ) ) ;
#13902=CIRCLE ( 'NONE', #38258, 2.055000000000000160 ) ;
#13932=LINE ( 'NONE', #40499, #17950 ) ;
#14030=ORIENTED_EDGE ( 'NONE', *, *, #226, .F. ) ;
#14143=CYLINDRICAL_SURFACE ( 'NONE', #34661, 4.250000000000000000 ) ;
#14167=ADVANCED_FACE ( 'NONE', ( #4377 ), #6036, .F. ) ;
#14185=APPLICATION_CONTEXT ( 'automotive_design' ) ;
#14207=EDGE_LOOP ( 'NONE', ( #31601, #14704, #32985, #29410 ) ) ;
#14223=VERTEX_POINT ( 'NONE', #34725 ) ;
#14252=DIRECTION ( 'NONE',  ( -0.000000000000000000, 1.000000000000000000, 1.224646799147353207E-16 ) ) ;
#14257=AXIS2_PLACEMENT_3D ( 'NONE', #12379, #22228, #35472 ) ;
#14425=DIRECTION ( 'NONE',  ( 1.000000000000000000, 0.000000000000000000, 0.000000000000000000 ) ) ;
#14469=TOROIDAL_SURFACE ( 'NONE', #31188, 4.000000000000000000, 0.2500000000000000000 ) ;
#14525=DIRECTION ( 'NONE',  ( 0.000000000000000000, 0.000000000000000000, 1.000000000000000000 ) ) ;
#14548=FILL_AREA_STYLE ('',( #25242 ) ) ;
#14597=DIRECTION ( 'NONE',  ( 0.000000000000000000, 0.000000000000000000, 1.000000000000000000 ) ) ;
#14609=LINE ( 'NONE', #4090, #39767 ) ;
#14622=VECTOR ( 'NONE', #26914, 999.9999999999997726 ) ;
#14628=CARTESIAN_POINT ( 'NONE',  ( 2.500000000000000000, 2.357898499370431722, -2.818925648462311528E-15 ) ) ;
#14632=ADVANCED_FACE ( 'NONE', ( #4493 ), #14143, .T. ) ;
#14690=DIRECTION ( 'NONE',  ( -1.000000000000000000, -0.000000000000000000, -0.000000000000000000 ) ) ;
#14700=DIRECTION ( 'NONE',  ( 0.000000000000000000, 0.000000000000000000, 1.000000000000000000 ) ) ;
#14704=ORIENTED_EDGE ( 'NONE', *, *, #28137, .T. ) ;
#14713=CIRCLE ( 'NONE', #15436, 4.000000000000000000 ) ;
#14777=CIRCLE ( 'NONE', #97, 2.041999999999999815 ) ;
#14807=DIRECTION ( 'NONE',  ( 0.000000000000000000, 0.000000000000000000, 1.000000000000000000 ) ) ;
#14871=ORIENTED_EDGE ( 'NONE', *, *, #28371, .F. ) ;
#14980=FACE_OUTER_BOUND ( 'NONE', #9138, .T. ) ;
#15059=ORIENTED_EDGE ( 'NONE', *, *, #15856, .F. ) ;
#15072=VECTOR ( 'NONE', #26311, 1000.000000000000114 ) ;
#15095=ORIENTED_EDGE ( 'NONE', *, *, #12108, .F. ) ;
#15161=CARTESIAN_POINT ( 'NONE',  ( -31.74999999999995737, 0.000000000000000000, 0.000000000000000000 ) ) ;
#15162=ORIENTED_EDGE ( 'NONE', *, *, #29483, .F. ) ;
#15193=LINE ( 'NONE', #42595, #24813 ) ;
#15196=ORIENTED_EDGE ( 'NONE', *, *, #40856, .F. ) ;
#15211=SURFACE_STYLE_USAGE ( .BOTH. , #4913 ) ;
#15249=ORIENTED_EDGE ( 'NONE', *, *, #28371, .T. ) ;
#15252=FACE_OUTER_BOUND ( 'NONE', #30204, .T. ) ;
#15273=DIRECTION ( 'NONE',  ( -1.000000000000000000, -0.000000000000000000, -0.000000000000000000 ) ) ;
#15313=DIRECTION ( 'NONE',  ( 0.000000000000000000, -1.000000000000000000, 1.287488025362403787E-15 ) ) ;
#15316=DIRECTION ( 'NONE',  ( 0.000000000000000000, 0.5000000000000009992, 0.8660254037844380415 ) ) ;
#15379=EDGE_LOOP ( 'NONE', ( #33448, #3202, #831 ) ) ;
#15388=FACE_OUTER_BOUND ( 'NONE', #27604, .T. ) ;
#15433=CIRCLE ( 'NONE', #23800, 2.041999999999999815 ) ;
#15436=AXIS2_PLACEMENT_3D ( 'NONE', #25441, #12757, #12121 ) ;
#15556=ORIENTED_EDGE ( 'NONE', *, *, #19844, .T. ) ;
#15621=EDGE_LOOP ( 'NONE', ( #17231, #2770, #19607, #37391 ) ) ;
#15643=EDGE_LOOP ( 'NONE', ( #15249, #38276, #12633 ) ) ;
#15856=EDGE_CURVE ( 'NONE', #30953, #12005, #35378, .T. ) ;
#15874=LINE ( 'NONE', #26744, #28523 ) ;
#15890=CIRCLE ( 'NONE', #28445, 2.041999999999999815 ) ;
#15893=ADVANCED_FACE ( 'NONE', ( #31683 ), #14469, .T. ) ;
#16147=ADVANCED_FACE ( 'NONE', ( #17713 ), #37305, .F. ) ;
#16405=CARTESIAN_POINT ( 'NONE',  ( 2.500000000000000000, -2.357898499370432166, 3.035766082959412415E-15 ) ) ;
#16424=SURFACE_STYLE_USAGE ( .BOTH. , #39929 ) ;
#16550=PRODUCT_DEFINITION_SHAPE ( 'NONE', 'NONE',  #4380 ) ;
#16582=AXIS2_PLACEMENT_3D ( 'NONE', #3337, #40625, #7489 ) ;
#16666=ORIENTED_EDGE ( 'NONE', *, *, #7767, .T. ) ;
#16701=CARTESIAN_POINT ( 'NONE',  ( 21.00000000000000355, 0.000000000000000000, 2.055000000000000160 ) ) ;
#16732=EDGE_CURVE ( 'NONE', #37953, #21211, #29574, .T. ) ;
#16756=ADVANCED_FACE ( 'NONE', ( #29157 ), #39398, .F. ) ;
#16782=ORIENTED_EDGE ( 'NONE', *, *, #15856, .T. ) ;
#16857=CARTESIAN_POINT ( 'NONE',  ( 2.500000000000000000, -1.178949249685214307, 2.042000000000001592 ) ) ;
#16861=DIRECTION ( 'NONE',  ( 0.000000000000000000, -0.4999999999999993339, 0.8660254037844390407 ) ) ;
#16996=EDGE_CURVE ( 'NONE', #20507, #25590, #34175, .T. ) ;
#17161=CIRCLE ( 'NONE', #22065, 2.500000000000000888 ) ;
#17231=ORIENTED_EDGE ( 'NONE', *, *, #23345, .F. ) ;
#17291=VECTOR ( 'NONE', #10968, 999.9999999999997726 ) ;
#17563=CARTESIAN_POINT ( 'NONE',  ( 2.500000000000000000, -2.357898499370432166, 3.035766082959412415E-15 ) ) ;
#17618=ORIENTED_EDGE ( 'NONE', *, *, #21006, .T. ) ;
#17662=AXIS2_PLACEMENT_3D ( 'NONE', #4985, #17908, #1696 ) ;
#17713=FACE_OUTER_BOUND ( 'NONE', #15643, .T. ) ;
#17765=DIRECTION ( 'NONE',  ( 0.000000000000000000, 0.8660254037844380415, -0.5000000000000012212 ) ) ;
#17815=DIRECTION ( 'NONE',  ( -1.000000000000000000, -0.000000000000000000, -0.000000000000000000 ) ) ;
#17868=CARTESIAN_POINT ( 'NONE',  ( -31.74999999999995737, 0.000000000000000000, 0.000000000000000000 ) ) ;
#17890=DIRECTION ( 'NONE',  ( 0.000000000000000000, 0.000000000000000000, -1.000000000000000000 ) ) ;
#17900=CARTESIAN_POINT ( 'NONE',  ( 0.2500000000000002220, 0.000000000000000000, 4.250000000000000000 ) ) ;
#17908=DIRECTION ( 'NONE',  ( 1.000000000000000000, 0.000000000000000000, 0.000000000000000000 ) ) ;
#17950=VECTOR ( 'NONE', #23325, 1000.000000000000114 ) ;
#17961=EDGE_CURVE ( 'NONE', #34610, #10833, #29783, .T. ) ;
#18009=SHAPE_REPRESENTATION ( 'socket head cap screw_iso_ISO 4762 M5 x 16 - 16N', ( #13552 ), #2321 ) ;
#18025=AXIS2_PLACEMENT_3D ( 'NONE', #10932, #14425, #21206 ) ;
#18135=EDGE_CURVE ( 'NONE', #9576, #22696, #37982, .T. ) ;
#18150=CARTESIAN_POINT ( 'NONE',  ( 2.500000000000000000, 0.000000000000000000, 0.000000000000000000 ) ) ;
#18151=ORIENTED_EDGE ( 'NONE', *, *, #1766, .T. ) ;
#18177=ORIENTED_EDGE ( 'NONE', *, *, #34171, .T. ) ;
#18196=AXIS2_PLACEMENT_3D ( 'NONE', #18150, #11567, #4553 ) ;
#18218=CARTESIAN_POINT ( 'NONE',  ( 3.678949249685231848, 0.000000000000000000, 0.000000000000000000 ) ) ;
#18273=PRESENTATION_STYLE_ASSIGNMENT (( #15211 ) ) ;
#18391=ORIENTED_EDGE ( 'NONE', *, *, #12108, .T. ) ;
#18394=EDGE_CURVE ( 'NONE', #967, #34610, #23166, .T. ) ;
#18422=CARTESIAN_POINT ( 'NONE',  ( 0.2500000000000002220, 0.000000000000000000, 0.000000000000000000 ) ) ;
#18439=ORIENTED_EDGE ( 'NONE', *, *, #6718, .F. ) ;
#18485=CARTESIAN_POINT ( 'NONE',  ( 2.500000000000000000, 0.000000000000000000, 0.000000000000000000 ) ) ;
#18530=CARTESIAN_POINT ( 'NONE',  ( -31.74999999999995737, 0.000000000000000000, 0.000000000000000000 ) ) ;
#18571=AXIS2_PLACEMENT_3D ( 'NONE', #31926, #11653, #8563 ) ;
#18573=ORIENTED_EDGE ( 'NONE', *, *, #38625, .T. ) ;
#18613=PRODUCT_CONTEXT ( 'NONE', #14185, 'mechanical' ) ;
#18614=EDGE_CURVE ( 'NONE', #33396, #20507, #6801, .T. ) ;
#18637=PLANE ( 'NONE',  #25639 ) ;
#18698=CIRCLE ( 'NONE', #16582, 4.250000000000000000 ) ;
#18774=AXIS2_PLACEMENT_3D ( 'NONE', #1827, #41753, #14525 ) ;
#18822=TOROIDAL_SURFACE ( 'NONE', #39671, 4.000000000000000000, 0.2500000000000000000 ) ;
#18946=EDGE_CURVE ( 'NONE', #10833, #21049, #26388, .T. ) ;
#19017=CARTESIAN_POINT ( 'NONE',  ( 2.500000000000000000, -1.178949249685214307, 2.042000000000001592 ) ) ;
#19065=CARTESIAN_POINT ( 'NONE',  ( 5.200000000000002842, 3.306546357697854226E-16, 2.700000000000000622 ) ) ;
#19089=CARTESIAN_POINT ( 'NONE',  ( 20.55500000000001748, 0.000000000000000000, 0.000000000000000000 ) ) ;
#19122=ADVANCED_FACE ( 'NONE', ( #38265 ), #25726, .T. ) ;
#19166=ORIENTED_EDGE ( 'NONE', *, *, #37415, .F. ) ;
#19279=EDGE_CURVE ( 'NONE', #41990, #28580, #38683, .T. ) ;
#19345=FACE_BOUND ( 'NONE', #49, .T. ) ;
#19462=CARTESIAN_POINT ( 'NONE',  ( -31.74999999999995737, 0.000000000000000000, 2.500000000000000444 ) ) ;
#19528=EDGE_CURVE ( 'NONE', #32115, #4308, #41474, .T. ) ;
#19575=ORIENTED_EDGE ( 'NONE', *, *, #38625, .F. ) ;
#19607=ORIENTED_EDGE ( 'NONE', *, *, #26538, .T. ) ;
#19774=CARTESIAN_POINT ( 'NONE',  ( 2.500000000000000000, 0.000000000000000000, 0.000000000000000000 ) ) ;
#19792=DIRECTION ( 'NONE',  ( -1.000000000000000000, -0.000000000000000000, -0.000000000000000000 ) ) ;
#19825=AXIS2_PLACEMENT_3D ( 'NONE', #42627, #22203, #12776 ) ;
#19844=EDGE_CURVE ( 'NONE', #8139, #42638, #4851, .T. ) ;
#19848=ADVANCED_FACE ( 'NONE', ( #26422 ), #12899, .F. ) ;
#19947=CARTESIAN_POINT ( 'NONE',  ( 2.500000000000000000, -2.357898499370432166, 3.035766082959412415E-15 ) ) ;
#20041=LINE ( 'NONE', #26988, #26516 ) ;
#20111=ORIENTED_EDGE ( 'NONE', *, *, #11978, .T. ) ;
#20114=DIRECTION ( 'NONE',  ( -1.000000000000000000, -0.000000000000000000, -0.000000000000000000 ) ) ;
#20137=FACE_OUTER_BOUND ( 'NONE', #11422, .T. ) ;
#20165=ORIENTED_EDGE ( 'NONE', *, *, #37005, .F. ) ;
#20224=DIRECTION ( 'NONE',  ( 0.000000000000000000, 0.000000000000000000, 1.000000000000000000 ) ) ;
#20225=CARTESIAN_POINT ( 'NONE',  ( 0.000000000000000000, 1.178949249685212974, -2.042000000000001148 ) ) ;
#20322=AXIS2_PLACEMENT_3D ( 'NONE', #33179, #26862, #17890 ) ;
#20406=CARTESIAN_POINT ( 'NONE',  ( 2.500000000000000000, 2.357898499370431722, -2.818925648462311528E-15 ) ) ;
#20436=ORIENTED_EDGE ( 'NONE', *, *, #28137, .F. ) ;
#20507=VERTEX_POINT ( 'NONE', #35476 ) ;
#20565=EDGE_CURVE ( 'NONE', #39739, #37953, #13902, .T. ) ;
#20634=LINE ( 'NONE', #27164, #35296 ) ;
#20754=EDGE_CURVE ( 'NONE', #28770, #10324, #15874, .T. ) ;
#21006=EDGE_CURVE ( 'NONE', #34092, #37795, #39728, .T. ) ;
#21037=DIRECTION ( 'NONE',  ( 0.000000000000000000, -0.5000000000000009992, -0.8660254037844380415 ) ) ;
#21046=CARTESIAN_POINT ( 'NONE',  ( 2.500000000000000000, 2.357898499370431722, -2.818925648462311528E-15 ) ) ;
#21049=VERTEX_POINT ( 'NONE', #23207 ) ;
#21060=ADVANCED_FACE ( 'NONE', ( #42575 ), #36244, .F. ) ;
#21096=CARTESIAN_POINT ( 'NONE',  ( 2.500000000000000000, 2.357898499370431722, -2.818925648462311528E-15 ) ) ;
#21206=DIRECTION ( 'NONE',  ( 0.000000000000000000, 0.000000000000000000, -1.000000000000000000 ) ) ;
#21211=VERTEX_POINT ( 'NONE', #27537 ) ;
#21261=PLANE ( 'NONE',  #32455 ) ;
#21328=( NAMED_UNIT ( * ) SI_UNIT ( $, .STERADIAN. ) SOLID_ANGLE_UNIT ( ) );
#21381=VECTOR ( 'NONE', #41349, 1000.000000000000000 ) ;
#21440=ORIENTED_EDGE ( 'NONE', *, *, #19528, .T. ) ;
#21482=DIRECTION ( 'NONE',  ( 1.000000000000000000, 0.000000000000000000, 0.000000000000000000 ) ) ;
#21582=CARTESIAN_POINT ( 'NONE',  ( 0.000000000000000000, -1.178949249685214307, 2.042000000000001592 ) ) ;
#21738=EDGE_LOOP ( 'NONE', ( #9298, #32847 ) ) ;
#21745=TOROIDAL_SURFACE ( 'NONE', #20322, 2.700000000000000622, 0.2000000000000000111 ) ;
#21824=EDGE_LOOP ( 'NONE', ( #13314, #29901, #34539, #30795, #18391 ) ) ;
#22018=DIRECTION ( 'NONE',  ( -1.000000000000000000, -0.000000000000000000, -0.000000000000000000 ) ) ;
#22065=AXIS2_PLACEMENT_3D ( 'NONE', #19089, #28888, #3241 ) ;
#22083=CIRCLE ( 'NONE', #26938, 2.700000000000000622 ) ;
#22203=DIRECTION ( 'NONE',  ( -1.000000000000000000, 0.000000000000000000, -0.000000000000000000 ) ) ;
#22228=DIRECTION ( 'NONE',  ( 1.000000000000000000, 0.000000000000000000, 0.000000000000000000 ) ) ;
#22325=VECTOR ( 'NONE', #13789, 1000.000000000000114 ) ;
#22342=CARTESIAN_POINT ( 'NONE',  ( 2.500000000000000000, 0.000000000000000000, 0.000000000000000000 ) ) ;
#22343=DIRECTION ( 'NONE',  ( 0.000000000000000000, 1.000000000000000000, -1.287488025362403787E-15 ) ) ;
#22527=ADVANCED_FACE ( 'NONE', ( #6229, #15252 ), #32638, .T. ) ;
#22549=ORIENTED_EDGE ( 'NONE', *, *, #226, .T. ) ;
#22557=VECTOR ( 'NONE', #13260, 1000.000000000000000 ) ;
#22652=EDGE_LOOP ( 'NONE', ( #33480, #15556 ) ) ;
#22696=VERTEX_POINT ( 'NONE', #20225 ) ;
#22899=VECTOR ( 'NONE', #33376, 1000.000000000000000 ) ;
#22927=EDGE_CURVE ( 'NONE', #21211, #10833, #40655, .T. ) ;
#23082=EDGE_CURVE ( 'NONE', #12005, #14223, #15193, .T. ) ;
#23166=LINE ( 'NONE', #19462, #22899 ) ;
#23187=FACE_OUTER_BOUND ( 'NONE', #37075, .T. ) ;
#23207=CARTESIAN_POINT ( 'NONE',  ( 5.000000000000002665, 0.000000000000000000, -2.700000000000000622 ) ) ;
#23325=DIRECTION ( 'NONE',  ( 0.000000000000000000, -0.5000000000000009992, -0.8660254037844380415 ) ) ;
#23340=ADVANCED_FACE ( 'NONE', ( #37351 ), #21261, .F. ) ;
#23345=EDGE_CURVE ( 'NONE', #25590, #8139, #10893, .T. ) ;
#23357=FACE_OUTER_BOUND ( 'NONE', #9939, .T. ) ;
#23366=CARTESIAN_POINT ( 'NONE',  ( 21.00000000000000355, 0.000000000000000000, 0.000000000000000000 ) ) ;
#23375=CARTESIAN_POINT ( 'NONE',  ( 0.000000000000000000, 0.000000000000000000, 0.000000000000000000 ) ) ;
#23415=CIRCLE ( 'NONE', #26199, 4.250000000000000000 ) ;
#23519=CONICAL_SURFACE ( 'NONE', #32546, 2.041999999999999815, 1.047197551196591858 ) ;
#23593=DIRECTION ( 'NONE',  ( 0.000000000000000000, 0.000000000000000000, 1.000000000000000000 ) ) ;
#23642=EDGE_LOOP ( 'NONE', ( #32856, #1142, #2520, #34005 ) ) ;
#23669=CARTESIAN_POINT ( 'NONE',  ( 2.500000000000000000, 2.357898499370431722, -2.818925648462311528E-15 ) ) ;
#23722=ORIENTED_EDGE ( 'NONE', *, *, #16996, .T. ) ;
#23800=AXIS2_PLACEMENT_3D ( 'NONE', #31762, #37848, #34155 ) ;
#23887=ADVANCED_FACE ( 'NONE', ( #4958 ), #34195, .T. ) ;
#24018=DIRECTION ( 'NONE',  ( -1.000000000000000000, -0.000000000000000000, -0.000000000000000000 ) ) ;
#24059=ORIENTED_EDGE ( 'NONE', *, *, #23082, .F. ) ;
#24117=ORIENTED_EDGE ( 'NONE', *, *, #4828, .F. ) ;
#24176=AXIS2_PLACEMENT_3D ( 'NONE', #18530, #27899, #14807 ) ;
#24187=DIRECTION ( 'NONE',  ( 0.000000000000000000, 0.000000000000000000, 1.000000000000000000 ) ) ;
#24362=DIRECTION ( 'NONE',  ( 0.000000000000000000, 0.4999999999999992784, -0.8660254037844389297 ) ) ;
#24399=ORIENTED_EDGE ( 'NONE', *, *, #4670, .F. ) ;
#24486=ADVANCED_FACE ( 'NONE', ( #14980 ), #23519, .F. ) ;
#24497=EDGE_CURVE ( 'NONE', #11322, #32708, #39363, .T. ) ;
#24556=DIRECTION ( 'NONE',  ( -1.000000000000000000, -0.000000000000000000, -0.000000000000000000 ) ) ;
#24569=VERTEX_POINT ( 'NONE', #9716 ) ;
#24575=PLANE ( 'NONE',  #6766 ) ;
#24582=ORIENTED_EDGE ( 'NONE', *, *, #1766, .F. ) ;
#24746=CARTESIAN_POINT ( 'NONE',  ( 0.2500000000000002220, 0.000000000000000000, 0.000000000000000000 ) ) ;
#24813=VECTOR ( 'NONE', #8383, 1000.000000000000000 ) ;
#24950=ORIENTED_EDGE ( 'NONE', *, *, #34726, .F. ) ;
#24956=CIRCLE ( 'NONE', #27701, 2.055000000000000160 ) ;
#25055=VECTOR ( 'NONE', #10036, 1000.000000000000000 ) ;
#25100=CARTESIAN_POINT ( 'NONE',  ( 0.2500000000000002220, 5.204748896376250699E-16, -4.250000000000000000 ) ) ;
#25137=CARTESIAN_POINT ( 'NONE',  ( 2.500000000000000000, -1.178949249685214307, 2.042000000000001592 ) ) ;
#25242=FILL_AREA_STYLE_COLOUR ( '', #40734 ) ;
#25258=AXIS2_PLACEMENT_3D ( 'NONE', #22342, #39504, #42131 ) ;
#25295=CARTESIAN_POINT ( 'NONE',  ( 2.500000000000000000, 0.000000000000000000, 0.000000000000000000 ) ) ;
#25351=ORIENTED_EDGE ( 'NONE', *, *, #6718, .T. ) ;
#25369=MECHANICAL_DESIGN_GEOMETRIC_PRESENTATION_REPRESENTATION('',(#220),#2995);
#25403=( LENGTH_UNIT ( ) NAMED_UNIT ( * ) SI_UNIT ( .MILLI., .METRE. ) );
#25441=CARTESIAN_POINT ( 'NONE',  ( 0.000000000000000000, 0.000000000000000000, 0.000000000000000000 ) ) ;
#25559=PLANE ( 'NONE',  #398 ) ;
#25590=VERTEX_POINT ( 'NONE', #25100 ) ;
#25610=ORIENTED_EDGE ( 'NONE', *, *, #31463, .F. ) ;
#25639=AXIS2_PLACEMENT_3D ( 'NONE', #8537, #21482, #31472 ) ;
#25726=CONICAL_SURFACE ( 'NONE', #18774, 2.055000000000000160, 0.7853981633974639331 ) ;
#25792=ORIENTED_EDGE ( 'NONE', *, *, #34243, .T. ) ;
#25882=EDGE_CURVE ( 'NONE', #34092, #9576, #323, .T. ) ;
#25884=FACE_OUTER_BOUND ( 'NONE', #22652, .T. ) ;
#26019=ORIENTED_EDGE ( 'NONE', *, *, #25882, .F. ) ;
#26067=ORIENTED_EDGE ( 'NONE', *, *, #27930, .F. ) ;
#26175=VECTOR ( 'NONE', #7071, 1000.000000000000114 ) ;
#26199=AXIS2_PLACEMENT_3D ( 'NONE', #8801, #38898, #23593 ) ;
#26311=DIRECTION ( 'NONE',  ( -0.7071067811865364705, 8.659560562355067211E-17, -0.7071067811865584529 ) ) ;
#26388=CIRCLE ( 'NONE', #8256, 0.2000000000000000944 ) ;
#26422=FACE_OUTER_BOUND ( 'NONE', #15379, .T. ) ;
#26502=ORIENTED_EDGE ( 'NONE', *, *, #28220, .T. ) ;
#26516=VECTOR ( 'NONE', #33076, 1000.000000000000114 ) ;
#26534=CYLINDRICAL_SURFACE ( 'NONE', #5474, 2.500000000000000444 ) ;
#26538=EDGE_CURVE ( 'NONE', #40845, #42638, #31615, .T. ) ;
#26557=VECTOR ( 'NONE', #41055, 1000.000000000000114 ) ;
#26637=VERTEX_POINT ( 'NONE', #28412 ) ;
#26702=CARTESIAN_POINT ( 'NONE',  ( 2.500000000000000000, -2.629050547790028551E-15, -2.041999999999999815 ) ) ;
#26744=CARTESIAN_POINT ( 'NONE',  ( 2.500000000000000000, 1.178949249685212974, -2.042000000000001148 ) ) ;
#26764=CARTESIAN_POINT ( 'NONE',  ( 2.500000000000000000, 2.357898499370431722, -2.818925648462311528E-15 ) ) ;
#26769=ORIENTED_EDGE ( 'NONE', *, *, #41442, .F. ) ;
#26824=CARTESIAN_POINT ( 'NONE',  ( 2.500000000000000000, 2.357898499370431722, -2.818925648462311528E-15 ) ) ;
#26862=DIRECTION ( 'NONE',  ( 1.000000000000000000, 0.000000000000000000, 0.000000000000000000 ) ) ;
#26895=DIRECTION ( 'NONE',  ( 0.000000000000000000, 0.000000000000000000, -1.000000000000000000 ) ) ;
#26914=DIRECTION ( 'NONE',  ( 0.000000000000000000, -0.5000000000000013323, -0.8660254037844380415 ) ) ;
#26938=AXIS2_PLACEMENT_3D ( 'NONE', #38020, #27812, #41063 ) ;
#26959=CARTESIAN_POINT ( 'NONE',  ( 21.00000000000000355, 0.000000000000000000, 0.000000000000000000 ) ) ;
#26977=CARTESIAN_POINT ( 'NONE',  ( 2.500000000000000000, -1.178949249685214307, 2.042000000000001592 ) ) ;
#26988=CARTESIAN_POINT ( 'NONE',  ( 2.500000000000000000, 0.000000000000000000, 2.041999999999999815 ) ) ;
#27120=CARTESIAN_POINT ( 'NONE',  ( 5.200000000000002842, 0.000000000000000000, 0.000000000000000000 ) ) ;
#27164=CARTESIAN_POINT ( 'NONE',  ( 0.000000000000000000, -2.357898499370432166, 3.035766082959412415E-15 ) ) ;
#27227=CARTESIAN_POINT ( 'NONE',  ( 5.200000000000002842, 0.000000000000000000, 2.500000000000000444 ) ) ;
#27274=CARTESIAN_POINT ( 'NONE',  ( 4.999999999999997335, 0.000000000000000000, 0.000000000000000000 ) ) ;
#27396=ORIENTED_EDGE ( 'NONE', *, *, #16996, .F. ) ;
#27537=CARTESIAN_POINT ( 'NONE',  ( 20.55500000000001748, 3.061616997868384127E-16, -2.500000000000000888 ) ) ;
#27568=LINE ( 'NONE', #17563, #26557 ) ;
#27604=EDGE_LOOP ( 'NONE', ( #29311, #3642, #8396, #20436 ) ) ;
#27693=CARTESIAN_POINT ( 'NONE',  ( 2.500000000000000000, 0.000000000000000000, 0.000000000000000000 ) ) ;
#27701=AXIS2_PLACEMENT_3D ( 'NONE', #26959, #36524, #20224 ) ;
#27795=DIRECTION ( 'NONE',  ( -1.000000000000000000, -0.000000000000000000, -0.000000000000000000 ) ) ;
#27812=DIRECTION ( 'NONE',  ( -1.000000000000000000, -0.000000000000000000, -0.000000000000000000 ) ) ;
#27899=DIRECTION ( 'NONE',  ( -1.000000000000000000, -0.000000000000000000, -0.000000000000000000 ) ) ;
#27900=CARTESIAN_POINT ( 'NONE',  ( 0.000000000000000000, 2.357898499370431722, -2.818925648462311528E-15 ) ) ;
#27930=EDGE_CURVE ( 'NONE', #32170, #10324, #4220, .T. ) ;
#27954=ORIENTED_EDGE ( 'NONE', *, *, #4204, .F. ) ;
#27995=ORIENTED_EDGE ( 'NONE', *, *, #3346, .F. ) ;
#28007=FACE_OUTER_BOUND ( 'NONE', #23642, .T. ) ;
#28137=EDGE_CURVE ( 'NONE', #21211, #967, #17161, .T. ) ;
#28197=ADVANCED_FACE ( 'NONE', ( #15388 ), #33848, .T. ) ;
#28220=EDGE_CURVE ( 'NONE', #25590, #40845, #23415, .T. ) ;
#28266=( GEOMETRIC_REPRESENTATION_CONTEXT ( 3 ) GLOBAL_UNCERTAINTY_ASSIGNED_CONTEXT ( ( #42237 ) ) GLOBAL_UNIT_ASSIGNED_CONTEXT ( ( #1625, #2629, #21328 ) ) REPRESENTATION_CONTEXT ( 'NONE', 'WORKASPACE' ) );
#28291=DIRECTION ( 'NONE',  ( -1.000000000000000000, -0.000000000000000000, -0.000000000000000000 ) ) ;
#28316=LINE ( 'NONE', #21582, #29271 ) ;
#28349=DIRECTION ( 'NONE',  ( 0.000000000000000000, 0.000000000000000000, 1.000000000000000000 ) ) ;
#28371=EDGE_CURVE ( 'NONE', #12884, #28770, #30758, .T. ) ;
#28412=CARTESIAN_POINT ( 'NONE',  ( 0.000000000000000000, -1.178949249685218748, -2.041999999999998039 ) ) ;
#28445=AXIS2_PLACEMENT_3D ( 'NONE', #27693, #33561, #3648 ) ;
#28453=DIRECTION ( 'NONE',  ( 0.000000000000000000, 1.000000000000000000, -1.224646799147353207E-16 ) ) ;
#28523=VECTOR ( 'NONE', #82, 1000.000000000000000 ) ;
#28547=DIRECTION ( 'NONE',  ( 0.000000000000000000, 0.000000000000000000, 1.000000000000000000 ) ) ;
#28553=AXIS2_PLACEMENT_3D ( 'NONE', #33206, #39938, #6799 ) ;
#28580=VERTEX_POINT ( 'NONE', #1494 ) ;
#28667=CYLINDRICAL_SURFACE ( 'NONE', #30406, 2.500000000000000444 ) ;
#28682=DIRECTION ( 'NONE',  ( 0.000000000000000000, 0.000000000000000000, 1.000000000000000000 ) ) ;
#28686=LINE ( 'NONE', #19947, #11180 ) ;
#28690=CARTESIAN_POINT ( 'NONE',  ( 2.500000000000000000, -2.357898499370432166, 3.035766082959412415E-15 ) ) ;
#28770=VERTEX_POINT ( 'NONE', #36807 ) ;
#28789=CIRCLE ( 'NONE', #17662, 4.250000000000000000 ) ;
#28803=EDGE_LOOP ( 'NONE', ( #38536, #31228, #39491 ) ) ;
#28871=( NAMED_UNIT ( * ) SI_UNIT ( $, .STERADIAN. ) SOLID_ANGLE_UNIT ( ) );
#28888=DIRECTION ( 'NONE',  ( -1.000000000000000000, -0.000000000000000000, -0.000000000000000000 ) ) ;
#28942=STYLED_ITEM ( 'NONE', ( #18273 ), #112 ) ;
#29092=ORIENTED_EDGE ( 'NONE', *, *, #3346, .T. ) ;
#29096=EDGE_LOOP ( 'NONE', ( #14030, #26019, #17618, #6765, #1843 ) ) ;
#29117=CARTESIAN_POINT ( 'NONE',  ( 21.00000000000000355, 0.000000000000000000, 2.055000000000000160 ) ) ;
#29157=FACE_OUTER_BOUND ( 'NONE', #4977, .T. ) ;
#29163=CARTESIAN_POINT ( 'NONE',  ( 2.500000000000000000, 1.178949249685212974, -2.042000000000001148 ) ) ;
#29173=VECTOR ( 'NONE', #2716, 1000.000000000000000 ) ;
#29200=DIRECTION ( 'NONE',  ( 1.000000000000000000, 0.000000000000000000, 0.000000000000000000 ) ) ;
#29271=VECTOR ( 'NONE', #41353, 1000.000000000000000 ) ;
#29311=ORIENTED_EDGE ( 'NONE', *, *, #16732, .F. ) ;
#29410=ORIENTED_EDGE ( 'NONE', *, *, #17961, .T. ) ;
#29483=EDGE_CURVE ( 'NONE', #39739, #967, #5541, .T. ) ;
#29574=LINE ( 'NONE', #42842, #15072 ) ;
#29659=DIRECTION ( 'NONE',  ( 0.000000000000000000, -1.000000000000000000, 1.287488025362403787E-15 ) ) ;
#29693=ADVANCED_BREP_SHAPE_REPRESENTATION ( '', ( #112, #13552 ), #2321 ) ;
#29706=DIRECTION ( 'NONE',  ( -0.000000000000000000, 0.8660254037844392627, 0.4999999999999990008 ) ) ;
#29708=VERTEX_POINT ( 'NONE', #21 ) ;
#29783=CIRCLE ( 'NONE', #39518, 2.500000000000000444 ) ;
#29798=ADVANCED_FACE ( 'NONE', ( #10977 ), #18637, .F. ) ;
#29808=CARTESIAN_POINT ( 'NONE',  ( 2.500000000000000000, -1.178949249685214307, 2.042000000000001592 ) ) ;
#29887=ORIENTED_EDGE ( 'NONE', *, *, #18135, .F. ) ;
#29891=CARTESIAN_POINT ( 'NONE',  ( 21.00000000000000355, 2.789133085058097101E-16, -2.055000000000000160 ) ) ;
#29901=ORIENTED_EDGE ( 'NONE', *, *, #36202, .F. ) ;
#29964=AXIS2_PLACEMENT_3D ( 'NONE', #16405, #29706, #3686 ) ;
#30163=DIRECTION ( 'NONE',  ( 0.000000000000000000, -0.4999999999999993339, 0.8660254037844390407 ) ) ;
#30204=EDGE_LOOP ( 'NONE', ( #13744, #24582 ) ) ;
#30294=AXIS2_PLACEMENT_3D ( 'NONE', #34540, #24556, #7926 ) ;
#30325=EDGE_CURVE ( 'NONE', #10324, #28580, #10146, .T. ) ;
#30330=EDGE_LOOP ( 'NONE', ( #8205, #37306, #10975, #15162 ) ) ;
#30406=AXIS2_PLACEMENT_3D ( 'NONE', #15161, #41936, #31500 ) ;
#30412=VECTOR ( 'NONE', #11340, 999.9999999999997726 ) ;
#30432=CIRCLE ( 'NONE', #11633, 2.041999999999999815 ) ;
#30435=AXIS2_PLACEMENT_3D ( 'NONE', #39945, #36682, #10076 ) ;
#30512=EDGE_LOOP ( 'NONE', ( #31910, #23722, #26502, #35450 ) ) ;
#30686=LINE ( 'NONE', #41112, #10942 ) ;
#30758=LINE ( 'NONE', #14628, #30412 ) ;
#30795=ORIENTED_EDGE ( 'NONE', *, *, #20754, .F. ) ;
#30863=CARTESIAN_POINT ( 'NONE',  ( 2.500000000000000000, 2.500728763858895382E-16, -2.041999999999999815 ) ) ;
#30925=CARTESIAN_POINT ( 'NONE',  ( 0.000000000000000000, 5.051668046482832750E-16, -4.000000000000000000 ) ) ;
#30953=VERTEX_POINT ( 'NONE', #40401 ) ;
#31161=VECTOR ( 'NONE', #21037, 1000.000000000000114 ) ;
#31188=AXIS2_PLACEMENT_3D ( 'NONE', #24746, #1780, #37997 ) ;
#31216=AXIS2_PLACEMENT_3D ( 'NONE', #27274, #24018, #8047 ) ;
#31228=ORIENTED_EDGE ( 'NONE', *, *, #19279, .F. ) ;
#31442=EDGE_LOOP ( 'NONE', ( #24950, #34684, #42062, #13549, #18573 ) ) ;
#31461=CARTESIAN_POINT ( 'NONE',  ( 0.000000000000000000, 2.357898499370431722, -2.818925648462311528E-15 ) ) ;
#31463=EDGE_CURVE ( 'NONE', #22696, #26637, #9578, .T. ) ;
#31472=DIRECTION ( 'NONE',  ( 0.000000000000000000, 0.000000000000000000, -1.000000000000000000 ) ) ;
#31500=DIRECTION ( 'NONE',  ( 0.000000000000000000, 0.000000000000000000, 1.000000000000000000 ) ) ;
#31601=ORIENTED_EDGE ( 'NONE', *, *, #22927, .F. ) ;
#31615=CIRCLE ( 'NONE', #37173, 0.2500000000000002220 ) ;
#31670=AXIS2_PLACEMENT_3D ( 'NONE', #19017, #41670, #15316 ) ;
#31683=FACE_OUTER_BOUND ( 'NONE', #15621, .T. ) ;
#31708=FACE_OUTER_BOUND ( 'NONE', #5495, .T. ) ;
#31762=CARTESIAN_POINT ( 'NONE',  ( 2.500000000000000000, 0.000000000000000000, 0.000000000000000000 ) ) ;
#31910=ORIENTED_EDGE ( 'NONE', *, *, #18614, .T. ) ;
#31926=CARTESIAN_POINT ( 'NONE',  ( 5.200000000000002842, 0.000000000000000000, 0.000000000000000000 ) ) ;
#32115=VERTEX_POINT ( 'NONE', #26977 ) ;
#32128=FACE_OUTER_BOUND ( 'NONE', #21824, .T. ) ;
#32156=DIRECTION ( 'NONE',  ( -0.7071067811865364705, 0.000000000000000000, 0.7071067811865584529 ) ) ;
#32165=ORIENTED_EDGE ( 'NONE', *, *, #37005, .T. ) ;
#32170=VERTEX_POINT ( 'NONE', #18218 ) ;
#32289=ORIENTED_EDGE ( 'NONE', *, *, #33539, .T. ) ;
#32455=AXIS2_PLACEMENT_3D ( 'NONE', #21046, #17765, #3961 ) ;
#32546=AXIS2_PLACEMENT_3D ( 'NONE', #18485, #28291, #3647 ) ;
#32638=PLANE ( 'NONE',  #14257 ) ;
#32666=DIRECTION ( 'NONE',  ( 0.000000000000000000, 0.000000000000000000, -1.000000000000000000 ) ) ;
#32708=VERTEX_POINT ( 'NONE', #5458 ) ;
#32732=DIRECTION ( 'NONE',  ( -1.000000000000000000, -0.000000000000000000, -0.000000000000000000 ) ) ;
#32760=FILL_AREA_STYLE_COLOUR ( '', #12827 ) ;
#32775=ADVANCED_FACE ( 'NONE', ( #41877 ), #25559, .T. ) ;
#32786=DIRECTION ( 'NONE',  ( 0.000000000000000000, 0.4999999999999990008, -0.8660254037844391517 ) ) ;
#32847=ORIENTED_EDGE ( 'NONE', *, *, #35108, .F. ) ;
#32856=ORIENTED_EDGE ( 'NONE', *, *, #28220, .F. ) ;
#32891=CARTESIAN_POINT ( 'NONE',  ( 5.200000000000002842, 0.000000000000000000, -2.700000000000000622 ) ) ;
#32985=ORIENTED_EDGE ( 'NONE', *, *, #18394, .T. ) ;
#33037=ORIENTED_EDGE ( 'NONE', *, *, #18394, .F. ) ;
#33058=DIRECTION ( 'NONE',  ( 0.000000000000000000, 0.000000000000000000, 1.000000000000000000 ) ) ;
#33076=DIRECTION ( 'NONE',  ( -0.5000000000000051070, 0.000000000000000000, 0.8660254037844355990 ) ) ;
#33179=CARTESIAN_POINT ( 'NONE',  ( 5.200000000000002842, 0.000000000000000000, 0.000000000000000000 ) ) ;
#33197=EDGE_CURVE ( 'NONE', #10324, #41990, #30432, .T. ) ;
#33206=CARTESIAN_POINT ( 'NONE',  ( 2.500000000000000000, 2.357898499370431722, -2.818925648462311528E-15 ) ) ;
#33360=EDGE_LOOP ( 'NONE', ( #20111, #24059, #15059, #15196, #21440 ) ) ;
#33376=DIRECTION ( 'NONE',  ( -1.000000000000000000, -0.000000000000000000, -0.000000000000000000 ) ) ;
#33384=CARTESIAN_POINT ( 'NONE',  ( 2.500000000000000000, 2.357898499370431722, -2.818925648462311528E-15 ) ) ;
#33396=VERTEX_POINT ( 'NONE', #9537 ) ;
#33448=ORIENTED_EDGE ( 'NONE', *, *, #10489, .F. ) ;
#33480=ORIENTED_EDGE ( 'NONE', *, *, #10182, .T. ) ;
#33539=EDGE_CURVE ( 'NONE', #33396, #40845, #30686, .T. ) ;
#33561=DIRECTION ( 'NONE',  ( -1.000000000000000000, -0.000000000000000000, -0.000000000000000000 ) ) ;
#33603=LINE ( 'NONE', #16857, #22325 ) ;
#33848=CONICAL_SURFACE ( 'NONE', #8748, 2.055000000000000160, 0.7853981633974639331 ) ;
#33871=ORIENTED_EDGE ( 'NONE', *, *, #18946, .F. ) ;
#34005=ORIENTED_EDGE ( 'NONE', *, *, #26538, .F. ) ;
#34092=VERTEX_POINT ( 'NONE', #20406 ) ;
#34155=DIRECTION ( 'NONE',  ( 0.000000000000000000, 0.000000000000000000, 1.000000000000000000 ) ) ;
#34171=EDGE_CURVE ( 'NONE', #10833, #34610, #12958, .T. ) ;
#34175=LINE ( 'NONE', #1871, #21381 ) ;
#34195=CYLINDRICAL_SURFACE ( 'NONE', #24176, 4.250000000000000000 ) ;
#34243=EDGE_CURVE ( 'NONE', #21049, #24569, #22083, .T. ) ;
#34508=DIRECTION ( 'NONE',  ( 0.000000000000000000, -1.224646799147353454E-16, 1.000000000000000000 ) ) ;
#34539=ORIENTED_EDGE ( 'NONE', *, *, #30325, .F. ) ;
#34540=CARTESIAN_POINT ( 'NONE',  ( 5.000000000000000888, 0.000000000000000000, 0.000000000000000000 ) ) ;
#34610=VERTEX_POINT ( 'NONE', #27227 ) ;
#34661=AXIS2_PLACEMENT_3D ( 'NONE', #17868, #11082, #24187 ) ;
#34684=ORIENTED_EDGE ( 'NONE', *, *, #19528, .F. ) ;
#34696=FACE_OUTER_BOUND ( 'NONE', #31442, .T. ) ;
#34714=EDGE_LOOP ( 'NONE', ( #16782, #24399, #26769 ) ) ;
#34725=CARTESIAN_POINT ( 'NONE',  ( 0.000000000000000000, 1.178949249685217415, 2.041999999999998483 ) ) ;
#34726=EDGE_CURVE ( 'NONE', #4308, #29708, #13932, .T. ) ;
#34871=CIRCLE ( 'NONE', #18196, 2.041999999999999815 ) ;
#34911=DIRECTION ( 'NONE',  ( 0.000000000000000000, 0.000000000000000000, -1.000000000000000000 ) ) ;
#34948=CARTESIAN_POINT ( 'NONE',  ( 2.500000000000000000, -1.178949249685214307, 2.042000000000001592 ) ) ;
#35108=EDGE_CURVE ( 'NONE', #37953, #39739, #24956, .T. ) ;
#35113=DIRECTION ( 'NONE',  ( -0.000000000000000000, 1.287488025362403787E-15, 1.000000000000000000 ) ) ;
#35296=VECTOR ( 'NONE', #43063, 1000.000000000000114 ) ;
#35306=ADVANCED_FACE ( 'NONE', ( #40882 ), #24575, .T. ) ;
#35378=LINE ( 'NONE', #34948, #43081 ) ;
#35450=ORIENTED_EDGE ( 'NONE', *, *, #33539, .F. ) ;
#35472=DIRECTION ( 'NONE',  ( 0.000000000000000000, 0.000000000000000000, -1.000000000000000000 ) ) ;
#35476=CARTESIAN_POINT ( 'NONE',  ( 4.999999999999997335, 5.204748896376250699E-16, -4.250000000000000000 ) ) ;
#35544=UNCERTAINTY_MEASURE_WITH_UNIT (LENGTH_MEASURE( 1.000000000000000082E-05 ), #36447, 'distance_accuracy_value', 'NONE');
#35600=ORIENTED_EDGE ( 'NONE', *, *, #27930, .T. ) ;
#35943=AXIS2_PLACEMENT_3D ( 'NONE', #19774, #36741, #43069 ) ;
#36040=ORIENTED_EDGE ( 'NONE', *, *, #5064, .T. ) ;
#36047=CARTESIAN_POINT ( 'NONE',  ( 2.500000000000000000, -1.768423874527823569, 1.021000000000002350 ) ) ;
#36102=DIRECTION ( 'NONE',  ( -1.000000000000000000, -0.000000000000000000, -0.000000000000000000 ) ) ;
#36202=EDGE_CURVE ( 'NONE', #28580, #26637, #39907, .T. ) ;
#36209=DIRECTION ( 'NONE',  ( 0.000000000000000000, 0.000000000000000000, 1.000000000000000000 ) ) ;
#36244=PLANE ( 'NONE',  #28553 ) ;
#36324=FACE_OUTER_BOUND ( 'NONE', #14207, .T. ) ;
#36342=LINE ( 'NONE', #2531, #5611 ) ;
#36414=ADVANCED_FACE ( 'NONE', ( #36324 ), #26534, .T. ) ;
#36447=( LENGTH_UNIT ( ) NAMED_UNIT ( * ) SI_UNIT ( .MILLI., .METRE. ) );
#36524=DIRECTION ( 'NONE',  ( -1.000000000000000000, -0.000000000000000000, -0.000000000000000000 ) ) ;
#36531=CARTESIAN_POINT ( 'NONE',  ( 2.500000000000000000, 1.178949249685212974, -2.042000000000001148 ) ) ;
#36560=VECTOR ( 'NONE', #16861, 1000.000000000000000 ) ;
#36618=PLANE ( 'NONE',  #13466 ) ;
#36656=AXIS2_PLACEMENT_3D ( 'NONE', #19065, #28453, #12286 ) ;
#36682=DIRECTION ( 'NONE',  ( 1.000000000000000000, 0.000000000000000000, 0.000000000000000000 ) ) ;
#36690=ORIENTED_EDGE ( 'NONE', *, *, #34243, .F. ) ;
#36741=DIRECTION ( 'NONE',  ( -1.000000000000000000, -0.000000000000000000, -0.000000000000000000 ) ) ;
#36807=CARTESIAN_POINT ( 'NONE',  ( 2.500000000000000000, 1.178949249685212974, -2.042000000000001148 ) ) ;
#37005=EDGE_CURVE ( 'NONE', #34092, #12884, #3530, .T. ) ;
#37053=ORIENTED_EDGE ( 'NONE', *, *, #4204, .T. ) ;
#37070=ADVANCED_FACE ( 'NONE', ( #28007 ), #18822, .T. ) ;
#37075=EDGE_LOOP ( 'NONE', ( #38891, #37053, #36690, #33871 ) ) ;
#37130=EDGE_LOOP ( 'NONE', ( #27396, #18151, #32289, #11089 ) ) ;
#37139=ORIENTED_EDGE ( 'NONE', *, *, #34171, .F. ) ;
#37173=AXIS2_PLACEMENT_3D ( 'NONE', #38609, #42091, #8730 ) ;
#37262=ORIENTED_EDGE ( 'NONE', *, *, #10873, .F. ) ;
#37305=PLANE ( 'NONE',  #18025 ) ;
#37306=ORIENTED_EDGE ( 'NONE', *, *, #16732, .T. ) ;
#37351=FACE_OUTER_BOUND ( 'NONE', #43078, .T. ) ;
#37362=ORIENTED_EDGE ( 'NONE', *, *, #33197, .T. ) ;
#37388=ADVANCED_FACE ( 'NONE', ( #20137 ), #13565, .T. ) ;
#37391=ORIENTED_EDGE ( 'NONE', *, *, #19844, .F. ) ;
#37415=EDGE_CURVE ( 'NONE', #32115, #11322, #33603, .T. ) ;
#37755=CIRCLE ( 'NONE', #25258, 2.041999999999999815 ) ;
#37795=VERTEX_POINT ( 'NONE', #1952 ) ;
#37848=DIRECTION ( 'NONE',  ( -1.000000000000000000, -0.000000000000000000, -0.000000000000000000 ) ) ;
#37849=ADVANCED_FACE ( 'NONE', ( #41666 ), #11812, .F. ) ;
#37904=PRODUCT_DEFINITION_FORMATION_WITH_SPECIFIED_SOURCE ( 'ANY', '', #3607, .NOT_KNOWN. ) ;
#37953=VERTEX_POINT ( 'NONE', #29891 ) ;
#37982=LINE ( 'NONE', #31461, #17291 ) ;
#37997=DIRECTION ( 'NONE',  ( 0.000000000000000000, 0.000000000000000000, 1.000000000000000000 ) ) ;
#38020=CARTESIAN_POINT ( 'NONE',  ( 5.000000000000000888, 0.000000000000000000, 0.000000000000000000 ) ) ;
#38032=ORIENTED_EDGE ( 'NONE', *, *, #21006, .F. ) ;
#38097=CARTESIAN_POINT ( 'NONE',  ( 2.500000000000000000, 1.178949249685217415, 2.041999999999998483 ) ) ;
#38198=AXIS2_PLACEMENT_3D ( 'NONE', #23375, #32732, #36209 ) ;
#38222=DIRECTION ( 'NONE',  ( 0.000000000000000000, 1.000000000000000000, -1.287488025362403787E-15 ) ) ;
#38258=AXIS2_PLACEMENT_3D ( 'NONE', #11959, #2092, #28547 ) ;
#38265=FACE_OUTER_BOUND ( 'NONE', #30330, .T. ) ;
#38276=ORIENTED_EDGE ( 'NONE', *, *, #20754, .T. ) ;
#38332=DIRECTION ( 'NONE',  ( 0.000000000000000000, 0.000000000000000000, 1.000000000000000000 ) ) ;
#38536=ORIENTED_EDGE ( 'NONE', *, *, #30325, .T. ) ;
#38608=SHAPE_DEFINITION_REPRESENTATION ( #16550, #18009 ) ;
#38609=CARTESIAN_POINT ( 'NONE',  ( 0.2500000000000002220, 0.000000000000000000, 4.000000000000000000 ) ) ;
#38625=EDGE_CURVE ( 'NONE', #32708, #29708, #28686, .T. ) ;
#38683=LINE ( 'NONE', #28690, #13154 ) ;
#38815=CARTESIAN_POINT ( 'NONE',  ( 21.00000000000000000, 2.055000000000000160, 0.000000000000000000 ) ) ;
#38891=ORIENTED_EDGE ( 'NONE', *, *, #17961, .F. ) ;
#38898=DIRECTION ( 'NONE',  ( 1.000000000000000000, 0.000000000000000000, 0.000000000000000000 ) ) ;
#39023=DIRECTION ( 'NONE',  ( 1.000000000000000000, 0.000000000000000000, 0.000000000000000000 ) ) ;
#39080=PLANE ( 'NONE',  #12875 ) ;
#39085=( NAMED_UNIT ( * ) PLANE_ANGLE_UNIT ( ) SI_UNIT ( $, .RADIAN. ) );
#39143=PLANE ( 'NONE',  #19825 ) ;
#39363=LINE ( 'NONE', #29808, #31161 ) ;
#39378=CARTESIAN_POINT ( 'NONE',  ( -31.74999999999995737, 0.000000000000000000, 0.000000000000000000 ) ) ;
#39398=CONICAL_SURFACE ( 'NONE', #35943, 2.041999999999999815, 1.047197551196591858 ) ;
#39491=ORIENTED_EDGE ( 'NONE', *, *, #33197, .F. ) ;
#39504=DIRECTION ( 'NONE',  ( -1.000000000000000000, -0.000000000000000000, -0.000000000000000000 ) ) ;
#39505=DIRECTION ( 'NONE',  ( 0.000000000000000000, -1.287488025362403787E-15, -1.000000000000000000 ) ) ;
#39518=AXIS2_PLACEMENT_3D ( 'NONE', #27120, #39733, #26895 ) ;
#39653=DIRECTION ( 'NONE',  ( -1.000000000000000000, -0.000000000000000000, -0.000000000000000000 ) ) ;
#39671=AXIS2_PLACEMENT_3D ( 'NONE', #18422, #27795, #14700 ) ;
#39718=PRESENTATION_STYLE_ASSIGNMENT (( #16424 ) ) ;
#39728=LINE ( 'NONE', #13163, #7611 ) ;
#39733=DIRECTION ( 'NONE',  ( 1.000000000000000000, 0.000000000000000000, 0.000000000000000000 ) ) ;
#39739=VERTEX_POINT ( 'NONE', #16701 ) ;
#39767=VECTOR ( 'NONE', #42185, 1000.000000000000000 ) ;
#39838=ORIENTED_EDGE ( 'NONE', *, *, #18135, .T. ) ;
#39907=LINE ( 'NONE', #12905, #25055 ) ;
#39919=CARTESIAN_POINT ( 'NONE',  ( 0.000000000000000000, 2.357898499370431722, -2.818925648462311528E-15 ) ) ;
#39929=SURFACE_SIDE_STYLE ('',( #42569 ) ) ;
#39938=DIRECTION ( 'NONE',  ( 1.000000000000000000, 0.000000000000000000, 0.000000000000000000 ) ) ;
#39945=CARTESIAN_POINT ( 'NONE',  ( 5.200000000000002842, 0.000000000000000000, 0.000000000000000000 ) ) ;
#40023=VECTOR ( 'NONE', #17815, 1000.000000000000000 ) ;
#40362=AXIS2_PLACEMENT_3D ( 'NONE', #33384, #2816, #9618 ) ;
#40401=CARTESIAN_POINT ( 'NONE',  ( 2.500000000000000000, 2.629050547790028946E-15, 2.042000000000000259 ) ) ;
#40499=CARTESIAN_POINT ( 'NONE',  ( 0.000000000000000000, -1.178949249685214307, 2.042000000000001592 ) ) ;
#40625=DIRECTION ( 'NONE',  ( -1.000000000000000000, -0.000000000000000000, -0.000000000000000000 ) ) ;
#40655=LINE ( 'NONE', #4678, #40023 ) ;
#40734=COLOUR_RGB ( '', 0.09019608, 0.27058824, 0.51372549) ;
#40823=CARTESIAN_POINT ( 'NONE',  ( 2.500000000000000000, -1.178949249685214307, 2.042000000000001592 ) ) ;
#40828=CARTESIAN_POINT ( 'NONE',  ( 0.2500000000000002220, 4.898587196589412829E-16, -4.000000000000000000 ) ) ;
#40845=VERTEX_POINT ( 'NONE', #17900 ) ;
#40856=EDGE_CURVE ( 'NONE', #32115, #30953, #14609, .T. ) ;
#40882=FACE_OUTER_BOUND ( 'NONE', #29096, .T. ) ;
#41055=DIRECTION ( 'NONE',  ( 0.000000000000000000, 0.4999999999999990008, -0.8660254037844391517 ) ) ;
#41063=DIRECTION ( 'NONE',  ( 0.000000000000000000, 0.000000000000000000, -1.000000000000000000 ) ) ;
#41112=CARTESIAN_POINT ( 'NONE',  ( -31.74999999999995737, 0.000000000000000000, 4.250000000000000000 ) ) ;
#41262=CIRCLE ( 'NONE', #41979, 2.500000000000000888 ) ;
#41349=DIRECTION ( 'NONE',  ( -1.000000000000000000, -0.000000000000000000, -0.000000000000000000 ) ) ;
#41353=DIRECTION ( 'NONE',  ( 0.000000000000000000, 1.000000000000000000, -1.287488025362403787E-15 ) ) ;
#41442=EDGE_CURVE ( 'NONE', #30953, #37795, #37755, .T. ) ;
#41474=LINE ( 'NONE', #40823, #11099 ) ;
#41666=FACE_OUTER_BOUND ( 'NONE', #33360, .T. ) ;
#41670=DIRECTION ( 'NONE',  ( 0.000000000000000000, 0.8660254037844380415, -0.5000000000000009992 ) ) ;
#41753=DIRECTION ( 'NONE',  ( -1.000000000000000000, -0.000000000000000000, -0.000000000000000000 ) ) ;
#41877=FACE_OUTER_BOUND ( 'NONE', #21738, .T. ) ;
#41936=DIRECTION ( 'NONE',  ( -1.000000000000000000, -0.000000000000000000, -0.000000000000000000 ) ) ;
#41972=ORIENTED_EDGE ( 'NONE', *, *, #18946, .T. ) ;
#41979=AXIS2_PLACEMENT_3D ( 'NONE', #12441, #39653, #42288 ) ;
#41990=VERTEX_POINT ( 'NONE', #9363 ) ;
#42062=ORIENTED_EDGE ( 'NONE', *, *, #37415, .T. ) ;
#42091=DIRECTION ( 'NONE',  ( 0.000000000000000000, -1.000000000000000000, 0.000000000000000000 ) ) ;
#42130=ADVANCED_FACE ( 'NONE', ( #23357 ), #36618, .F. ) ;
#42131=DIRECTION ( 'NONE',  ( 0.000000000000000000, 0.000000000000000000, 1.000000000000000000 ) ) ;
#42185=DIRECTION ( 'NONE',  ( 0.000000000000000000, 1.000000000000000000, -1.287488025362403787E-15 ) ) ;
#42237=UNCERTAINTY_MEASURE_WITH_UNIT (LENGTH_MEASURE( 1.000000000000000082E-05 ), #1625, 'distance_accuracy_value', 'NONE');
#42288=DIRECTION ( 'NONE',  ( 0.000000000000000000, 0.000000000000000000, 1.000000000000000000 ) ) ;
#42290=EDGE_CURVE ( 'NONE', #40845, #25590, #28789, .T. ) ;
#42569=SURFACE_STYLE_FILL_AREA ( #13582 ) ;
#42575=FACE_OUTER_BOUND ( 'NONE', #34714, .T. ) ;
#42595=CARTESIAN_POINT ( 'NONE',  ( 2.500000000000000000, 1.178949249685217415, 2.041999999999998483 ) ) ;
#42627=CARTESIAN_POINT ( 'NONE',  ( 0.000000000000000000, 0.000000000000000000, 0.000000000000000000 ) ) ;
#42638=VERTEX_POINT ( 'NONE', #4475 ) ;
#42771=( NAMED_UNIT ( * ) SI_UNIT ( $, .STERADIAN. ) SOLID_ANGLE_UNIT ( ) );
#42796=DIRECTION ( 'NONE',  ( -1.000000000000000000, -0.000000000000000000, -0.000000000000000000 ) ) ;
#42842=CARTESIAN_POINT ( 'NONE',  ( 21.00000000000000355, 2.516649172247811061E-16, -2.055000000000000160 ) ) ;
#42849=ADVANCED_FACE ( 'NONE', ( #19345, #25884 ), #39143, .T. ) ;
#43063=DIRECTION ( 'NONE',  ( 0.000000000000000000, 0.4999999999999990008, -0.8660254037844391517 ) ) ;
#43069=DIRECTION ( 'NONE',  ( 0.000000000000000000, 0.000000000000000000, 1.000000000000000000 ) ) ;
#43078=EDGE_LOOP ( 'NONE', ( #39838, #15095, #14871, #20165, #2387 ) ) ;
#43081=VECTOR ( 'NONE', #38222, 1000.000000000000000 ) ;
ENDSEC;
END-ISO-10303-21;
